ISO-10303-21;
HEADER;
/* Generated by software containing ST-Developer
 * from STEP Tools, Inc. (www.steptools.com) 
 */

FILE_DESCRIPTION(
/* description */ ('Jaw-coupled motor to shaft test stand'),
/* implementation_level */ '2;1');

FILE_NAME(
/* name */ 'M3x10 motor screw (1).step',
/* time_stamp */ '2026-10-27T10:46:06-07:00',
/* author */ (''),
/* organization */ (''),
/* preprocessor_version */ 'ST-DEVELOPER v20.2',
/* originating_system */ 'Autodesk Translation Framework v15.17.0.0',
/* authorisation */ '');

FILE_SCHEMA (('AUTOMOTIVE_DESIGN { 1 0 10303 214 3 1 1 }'));
ENDSEC;

DATA;
#10=MECHANICAL_DESIGN_GEOMETRIC_PRESENTATION_REPRESENTATION('',(#350),#19361);
#286=SHAPE_REPRESENTATION_RELATIONSHIP('SRR','None',#19500,#318);
#318=ADVANCED_BREP_SHAPE_REPRESENTATION('',(#383),#19336);
#350=STYLED_ITEM('',(#19753),#383);
#383=MANIFOLD_SOLID_BREP('Body1',#10994);
#446=FACE_BOUND('',#1777,.T.);
#447=FACE_BOUND('',#1780,.T.);
#571=PLANE('',#11528);
#572=PLANE('',#11529);
#573=PLANE('',#11530);
#574=PLANE('',#11531);
#575=PLANE('',#11532);
#576=PLANE('',#11533);
#577=PLANE('',#11534);
#578=PLANE('',#11535);
#579=PLANE('',#11540);
#580=PLANE('',#11543);
#1106=FACE_OUTER_BOUND('',#1769,.T.);
#1107=FACE_OUTER_BOUND('',#1770,.T.);
#1108=FACE_OUTER_BOUND('',#1771,.T.);
#1109=FACE_OUTER_BOUND('',#1772,.T.);
#1110=FACE_OUTER_BOUND('',#1773,.T.);
#1111=FACE_OUTER_BOUND('',#1774,.T.);
#1112=FACE_OUTER_BOUND('',#1775,.T.);
#1113=FACE_OUTER_BOUND('',#1776,.T.);
#1114=FACE_OUTER_BOUND('',#1778,.T.);
#1115=FACE_OUTER_BOUND('',#1779,.T.);
#1116=FACE_OUTER_BOUND('',#1781,.T.);
#1117=FACE_OUTER_BOUND('',#1782,.T.);
#1769=EDGE_LOOP('',(#7688,#7689,#7690,#7691));
#1770=EDGE_LOOP('',(#7692,#7693,#7694,#7695));
#1771=EDGE_LOOP('',(#7696,#7697,#7698,#7699));
#1772=EDGE_LOOP('',(#7700,#7701,#7702,#7703));
#1773=EDGE_LOOP('',(#7704,#7705,#7706,#7707));
#1774=EDGE_LOOP('',(#7708,#7709,#7710,#7711));
#1775=EDGE_LOOP('',(#7712,#7713,#7714,#7715,#7716,#7717));
#1776=EDGE_LOOP('',(#7718));
#1777=EDGE_LOOP('',(#7719));
#1778=EDGE_LOOP('',(#7720,#7721,#7722,#7723));
#1779=EDGE_LOOP('',(#7724));
#1780=EDGE_LOOP('',(#7725,#7726,#7727,#7728,#7729,#7730));
#1781=EDGE_LOOP('',(#7731,#7732,#7733,#7734));
#1782=EDGE_LOOP('',(#7735));
#2488=LINE('',#15812,#3641);
#2489=LINE('',#15814,#3642);
#2490=LINE('',#15816,#3643);
#2491=LINE('',#15817,#3644);
#2492=LINE('',#15820,#3645);
#2493=LINE('',#15822,#3646);
#2494=LINE('',#15823,#3647);
#2495=LINE('',#15826,#3648);
#2496=LINE('',#15828,#3649);
#2497=LINE('',#15829,#3650);
#2498=LINE('',#15832,#3651);
#2499=LINE('',#15834,#3652);
#2500=LINE('',#15835,#3653);
#2501=LINE('',#15838,#3654);
#2502=LINE('',#15840,#3655);
#2503=LINE('',#15841,#3656);
#2504=LINE('',#15843,#3657);
#2505=LINE('',#15844,#3658);
#2506=LINE('',#15854,#3659);
#2507=LINE('',#15858,#3660);
#3641=VECTOR('',#12765,1.);
#3642=VECTOR('',#12766,1.);
#3643=VECTOR('',#12767,1.);
#3644=VECTOR('',#12768,1.);
#3645=VECTOR('',#12771,1.);
#3646=VECTOR('',#12772,1.);
#3647=VECTOR('',#12773,1.);
#3648=VECTOR('',#12776,1.);
#3649=VECTOR('',#12777,1.);
#3650=VECTOR('',#12778,1.);
#3651=VECTOR('',#12781,1.);
#3652=VECTOR('',#12782,1.);
#3653=VECTOR('',#12783,1.);
#3654=VECTOR('',#12786,1.);
#3655=VECTOR('',#12787,1.);
#3656=VECTOR('',#12788,1.);
#3657=VECTOR('',#12791,1.);
#3658=VECTOR('',#12792,1.);
#3659=VECTOR('',#12805,0.275);
#3660=VECTOR('',#12810,0.15);
#4739=CIRCLE('',#11536,0.275);
#4740=CIRCLE('',#11537,0.15);
#4741=CIRCLE('',#11539,0.275);
#4742=CIRCLE('',#11542,0.15);
#5057=VERTEX_POINT('',#15810);
#5058=VERTEX_POINT('',#15811);
#5059=VERTEX_POINT('',#15813);
#5060=VERTEX_POINT('',#15815);
#5061=VERTEX_POINT('',#15819);
#5062=VERTEX_POINT('',#15821);
#5063=VERTEX_POINT('',#15825);
#5064=VERTEX_POINT('',#15827);
#5065=VERTEX_POINT('',#15831);
#5066=VERTEX_POINT('',#15833);
#5067=VERTEX_POINT('',#15837);
#5068=VERTEX_POINT('',#15839);
#5069=VERTEX_POINT('',#15847);
#5070=VERTEX_POINT('',#15849);
#5071=VERTEX_POINT('',#15852);
#5072=VERTEX_POINT('',#15857);
#6055=EDGE_CURVE('',#5057,#5058,#2488,.T.);
#6056=EDGE_CURVE('',#5059,#5057,#2489,.T.);
#6057=EDGE_CURVE('',#5059,#5060,#2490,.T.);
#6058=EDGE_CURVE('',#5060,#5058,#2491,.T.);
#6059=EDGE_CURVE('',#5058,#5061,#2492,.T.);
#6060=EDGE_CURVE('',#5060,#5062,#2493,.T.);
#6061=EDGE_CURVE('',#5062,#5061,#2494,.T.);
#6062=EDGE_CURVE('',#5061,#5063,#2495,.T.);
#6063=EDGE_CURVE('',#5062,#5064,#2496,.T.);
#6064=EDGE_CURVE('',#5064,#5063,#2497,.T.);
#6065=EDGE_CURVE('',#5063,#5065,#2498,.T.);
#6066=EDGE_CURVE('',#5064,#5066,#2499,.T.);
#6067=EDGE_CURVE('',#5066,#5065,#2500,.T.);
#6068=EDGE_CURVE('',#5065,#5067,#2501,.T.);
#6069=EDGE_CURVE('',#5066,#5068,#2502,.T.);
#6070=EDGE_CURVE('',#5068,#5067,#2503,.T.);
#6071=EDGE_CURVE('',#5067,#5057,#2504,.T.);
#6072=EDGE_CURVE('',#5068,#5059,#2505,.T.);
#6073=EDGE_CURVE('',#5069,#5069,#4739,.T.);
#6074=EDGE_CURVE('',#5070,#5070,#4740,.T.);
#6075=EDGE_CURVE('',#5071,#5071,#4741,.T.);
#6076=EDGE_CURVE('',#5071,#5069,#2506,.T.);
#6077=EDGE_CURVE('',#5070,#5072,#2507,.T.);
#6078=EDGE_CURVE('',#5072,#5072,#4742,.T.);
#7688=ORIENTED_EDGE('',*,*,#6055,.F.);
#7689=ORIENTED_EDGE('',*,*,#6056,.F.);
#7690=ORIENTED_EDGE('',*,*,#6057,.T.);
#7691=ORIENTED_EDGE('',*,*,#6058,.T.);
#7692=ORIENTED_EDGE('',*,*,#6059,.F.);
#7693=ORIENTED_EDGE('',*,*,#6058,.F.);
#7694=ORIENTED_EDGE('',*,*,#6060,.T.);
#7695=ORIENTED_EDGE('',*,*,#6061,.T.);
#7696=ORIENTED_EDGE('',*,*,#6062,.F.);
#7697=ORIENTED_EDGE('',*,*,#6061,.F.);
#7698=ORIENTED_EDGE('',*,*,#6063,.T.);
#7699=ORIENTED_EDGE('',*,*,#6064,.T.);
#7700=ORIENTED_EDGE('',*,*,#6065,.F.);
#7701=ORIENTED_EDGE('',*,*,#6064,.F.);
#7702=ORIENTED_EDGE('',*,*,#6066,.T.);
#7703=ORIENTED_EDGE('',*,*,#6067,.T.);
#7704=ORIENTED_EDGE('',*,*,#6068,.F.);
#7705=ORIENTED_EDGE('',*,*,#6067,.F.);
#7706=ORIENTED_EDGE('',*,*,#6069,.T.);
#7707=ORIENTED_EDGE('',*,*,#6070,.T.);
#7708=ORIENTED_EDGE('',*,*,#6071,.F.);
#7709=ORIENTED_EDGE('',*,*,#6070,.F.);
#7710=ORIENTED_EDGE('',*,*,#6072,.T.);
#7711=ORIENTED_EDGE('',*,*,#6056,.T.);
#7712=ORIENTED_EDGE('',*,*,#6063,.F.);
#7713=ORIENTED_EDGE('',*,*,#6060,.F.);
#7714=ORIENTED_EDGE('',*,*,#6057,.F.);
#7715=ORIENTED_EDGE('',*,*,#6072,.F.);
#7716=ORIENTED_EDGE('',*,*,#6069,.F.);
#7717=ORIENTED_EDGE('',*,*,#6066,.F.);
#7718=ORIENTED_EDGE('',*,*,#6073,.F.);
#7719=ORIENTED_EDGE('',*,*,#6074,.T.);
#7720=ORIENTED_EDGE('',*,*,#6075,.F.);
#7721=ORIENTED_EDGE('',*,*,#6076,.T.);
#7722=ORIENTED_EDGE('',*,*,#6073,.T.);
#7723=ORIENTED_EDGE('',*,*,#6076,.F.);
#7724=ORIENTED_EDGE('',*,*,#6075,.T.);
#7725=ORIENTED_EDGE('',*,*,#6065,.T.);
#7726=ORIENTED_EDGE('',*,*,#6068,.T.);
#7727=ORIENTED_EDGE('',*,*,#6071,.T.);
#7728=ORIENTED_EDGE('',*,*,#6055,.T.);
#7729=ORIENTED_EDGE('',*,*,#6059,.T.);
#7730=ORIENTED_EDGE('',*,*,#6062,.T.);
#7731=ORIENTED_EDGE('',*,*,#6074,.F.);
#7732=ORIENTED_EDGE('',*,*,#6077,.T.);
#7733=ORIENTED_EDGE('',*,*,#6078,.T.);
#7734=ORIENTED_EDGE('',*,*,#6077,.F.);
#7735=ORIENTED_EDGE('',*,*,#6078,.F.);
#10299=CYLINDRICAL_SURFACE('',#11538,0.275);
#10300=CYLINDRICAL_SURFACE('',#11541,0.15);
#10448=ADVANCED_FACE('',(#1106),#571,.F.);
#10449=ADVANCED_FACE('',(#1107),#572,.F.);
#10450=ADVANCED_FACE('',(#1108),#573,.F.);
#10451=ADVANCED_FACE('',(#1109),#574,.F.);
#10452=ADVANCED_FACE('',(#1110),#575,.F.);
#10453=ADVANCED_FACE('',(#1111),#576,.F.);
#10454=ADVANCED_FACE('',(#1112),#577,.T.);
#10455=ADVANCED_FACE('',(#1113,#446),#578,.F.);
#10456=ADVANCED_FACE('',(#1114),#10299,.T.);
#10457=ADVANCED_FACE('',(#1115,#447),#579,.T.);
#10458=ADVANCED_FACE('',(#1116),#10300,.T.);
#10459=ADVANCED_FACE('',(#1117),#580,.F.);
#10994=CLOSED_SHELL('',(#10448,#10449,#10450,#10451,#10452,#10453,#10454,
#10455,#10456,#10457,#10458,#10459));
#11527=AXIS2_PLACEMENT_3D('',#15808,#12761,#12762);
#11528=AXIS2_PLACEMENT_3D('',#15809,#12763,#12764);
#11529=AXIS2_PLACEMENT_3D('',#15818,#12769,#12770);
#11530=AXIS2_PLACEMENT_3D('',#15824,#12774,#12775);
#11531=AXIS2_PLACEMENT_3D('',#15830,#12779,#12780);
#11532=AXIS2_PLACEMENT_3D('',#15836,#12784,#12785);
#11533=AXIS2_PLACEMENT_3D('',#15842,#12789,#12790);
#11534=AXIS2_PLACEMENT_3D('',#15845,#12793,#12794);
#11535=AXIS2_PLACEMENT_3D('',#15846,#12795,#12796);
#11536=AXIS2_PLACEMENT_3D('',#15848,#12797,#12798);
#11537=AXIS2_PLACEMENT_3D('',#15850,#12799,#12800);
#11538=AXIS2_PLACEMENT_3D('',#15851,#12801,#12802);
#11539=AXIS2_PLACEMENT_3D('',#15853,#12803,#12804);
#11540=AXIS2_PLACEMENT_3D('',#15855,#12806,#12807);
#11541=AXIS2_PLACEMENT_3D('',#15856,#12808,#12809);
#11542=AXIS2_PLACEMENT_3D('',#15859,#12811,#12812);
#11543=AXIS2_PLACEMENT_3D('',#15860,#12813,#12814);
#12761=DIRECTION('axis',(0.,0.,1.));
#12762=DIRECTION('refdir',(1.,0.,0.));
#12763=DIRECTION('center_axis',(-0.866025403784438,0.,0.5));
#12764=DIRECTION('ref_axis',(0.5,0.,0.866025403784438));
#12765=DIRECTION('',(-0.5,0.,-0.866025403784438));
#12766=DIRECTION('',(0.,1.,0.));
#12767=DIRECTION('',(-0.5,0.,-0.866025403784438));
#12768=DIRECTION('',(0.,1.,0.));
#12769=DIRECTION('center_axis',(-0.866025403784438,0.,-0.5));
#12770=DIRECTION('ref_axis',(-0.5,0.,0.866025403784438));
#12771=DIRECTION('',(0.5,0.,-0.866025403784438));
#12772=DIRECTION('',(0.5,0.,-0.866025403784438));
#12773=DIRECTION('',(0.,1.,0.));
#12774=DIRECTION('center_axis',(0.,0.,-1.));
#12775=DIRECTION('ref_axis',(-1.,0.,0.));
#12776=DIRECTION('',(1.,0.,0.));
#12777=DIRECTION('',(1.,0.,0.));
#12778=DIRECTION('',(0.,1.,0.));
#12779=DIRECTION('center_axis',(0.866025403784439,0.,-0.499999999999999));
#12780=DIRECTION('ref_axis',(-0.499999999999999,0.,-0.866025403784439));
#12781=DIRECTION('',(0.499999999999999,0.,0.866025403784439));
#12782=DIRECTION('',(0.499999999999999,0.,0.866025403784439));
#12783=DIRECTION('',(0.,1.,0.));
#12784=DIRECTION('center_axis',(0.866025403784439,0.,0.499999999999999));
#12785=DIRECTION('ref_axis',(0.499999999999999,0.,-0.866025403784439));
#12786=DIRECTION('',(-0.499999999999999,0.,0.866025403784439));
#12787=DIRECTION('',(-0.499999999999999,0.,0.866025403784439));
#12788=DIRECTION('',(0.,1.,0.));
#12789=DIRECTION('center_axis',(0.,0.,1.));
#12790=DIRECTION('ref_axis',(1.,0.,0.));
#12791=DIRECTION('',(-1.,0.,0.));
#12792=DIRECTION('',(-1.,0.,0.));
#12793=DIRECTION('center_axis',(0.,1.,0.));
#12794=DIRECTION('ref_axis',(1.,0.,0.));
#12795=DIRECTION('center_axis',(0.,1.,0.));
#12796=DIRECTION('ref_axis',(1.,0.,0.));
#12797=DIRECTION('center_axis',(0.,1.,0.));
#12798=DIRECTION('ref_axis',(1.,0.,0.));
#12799=DIRECTION('center_axis',(0.,1.,0.));
#12800=DIRECTION('ref_axis',(1.,0.,0.));
#12801=DIRECTION('center_axis',(0.,1.,0.));
#12802=DIRECTION('ref_axis',(1.,0.,0.));
#12803=DIRECTION('center_axis',(0.,1.,0.));
#12804=DIRECTION('ref_axis',(1.,0.,0.));
#12805=DIRECTION('',(0.,-1.,0.));
#12806=DIRECTION('center_axis',(0.,1.,0.));
#12807=DIRECTION('ref_axis',(1.,0.,0.));
#12808=DIRECTION('center_axis',(0.,1.,0.));
#12809=DIRECTION('ref_axis',(1.,0.,0.));
#12810=DIRECTION('',(0.,-1.,0.));
#12811=DIRECTION('center_axis',(0.,1.,0.));
#12812=DIRECTION('ref_axis',(1.,0.,0.));
#12813=DIRECTION('center_axis',(0.,1.,0.));
#12814=DIRECTION('ref_axis',(1.,0.,0.));
#15808=CARTESIAN_POINT('',(0.,0.,0.));
#15809=CARTESIAN_POINT('Origin',(-1.69433756729741,-6.9,5.77));
#15810=CARTESIAN_POINT('',(-1.6221687836487,-6.7,5.895));
#15811=CARTESIAN_POINT('',(-1.69433756729741,-6.7,5.77));
#15812=CARTESIAN_POINT('',(-1.67629537138523,-6.7,5.80125));
#15813=CARTESIAN_POINT('',(-1.6221687836487,-6.9,5.895));
#15814=CARTESIAN_POINT('',(-1.6221687836487,-6.9,5.895));
#15815=CARTESIAN_POINT('',(-1.69433756729741,-6.9,5.77));
#15816=CARTESIAN_POINT('',(-1.6221687836487,-6.9,5.895));
#15817=CARTESIAN_POINT('',(-1.69433756729741,-6.9,5.77));
#15818=CARTESIAN_POINT('Origin',(-1.6221687836487,-6.9,5.645));
#15819=CARTESIAN_POINT('',(-1.6221687836487,-6.7,5.645));
#15820=CARTESIAN_POINT('',(-1.64021097956088,-6.7,5.67625));
#15821=CARTESIAN_POINT('',(-1.6221687836487,-6.9,5.645));
#15822=CARTESIAN_POINT('',(-1.69433756729741,-6.9,5.77));
#15823=CARTESIAN_POINT('',(-1.6221687836487,-6.9,5.645));
#15824=CARTESIAN_POINT('Origin',(-1.4778312163513,-6.9,5.645));
#15825=CARTESIAN_POINT('',(-1.4778312163513,-6.7,5.645));
#15826=CARTESIAN_POINT('',(-1.51391560817565,-6.7,5.645));
#15827=CARTESIAN_POINT('',(-1.4778312163513,-6.9,5.645));
#15828=CARTESIAN_POINT('',(-1.6221687836487,-6.9,5.645));
#15829=CARTESIAN_POINT('',(-1.4778312163513,-6.9,5.645));
#15830=CARTESIAN_POINT('Origin',(-1.40566243270259,-6.9,5.77));
#15831=CARTESIAN_POINT('',(-1.40566243270259,-6.7,5.77));
#15832=CARTESIAN_POINT('',(-1.42370462861477,-6.7,5.73875));
#15833=CARTESIAN_POINT('',(-1.40566243270259,-6.9,5.77));
#15834=CARTESIAN_POINT('',(-1.4778312163513,-6.9,5.645));
#15835=CARTESIAN_POINT('',(-1.40566243270259,-6.9,5.77));
#15836=CARTESIAN_POINT('Origin',(-1.4778312163513,-6.9,5.895));
#15837=CARTESIAN_POINT('',(-1.4778312163513,-6.7,5.895));
#15838=CARTESIAN_POINT('',(-1.45978902043912,-6.7,5.86375));
#15839=CARTESIAN_POINT('',(-1.4778312163513,-6.9,5.895));
#15840=CARTESIAN_POINT('',(-1.40566243270259,-6.9,5.77));
#15841=CARTESIAN_POINT('',(-1.4778312163513,-6.9,5.895));
#15842=CARTESIAN_POINT('Origin',(-1.6221687836487,-6.9,5.895));
#15843=CARTESIAN_POINT('',(-1.58608439182435,-6.7,5.895));
#15844=CARTESIAN_POINT('',(-1.4778312163513,-6.9,5.895));
#15845=CARTESIAN_POINT('Origin',(-1.55,-6.9,5.77));
#15846=CARTESIAN_POINT('Origin',(-1.55,-7.,5.77));
#15847=CARTESIAN_POINT('',(-1.825,-7.,5.77));
#15848=CARTESIAN_POINT('Origin',(-1.55,-7.,5.77));
#15849=CARTESIAN_POINT('',(-1.7,-7.,5.77));
#15850=CARTESIAN_POINT('Origin',(-1.55,-7.,5.77));
#15851=CARTESIAN_POINT('Origin',(-1.55,-7.,5.77));
#15852=CARTESIAN_POINT('',(-1.825,-6.7,5.77));
#15853=CARTESIAN_POINT('Origin',(-1.55,-6.7,5.77));
#15854=CARTESIAN_POINT('',(-1.825,-7.,5.77));
#15855=CARTESIAN_POINT('Origin',(-1.55,-6.7,5.77));
#15856=CARTESIAN_POINT('Origin',(-1.55,-8.,5.77));
#15857=CARTESIAN_POINT('',(-1.7,-8.,5.77));
#15858=CARTESIAN_POINT('',(-1.7,-8.,5.77));
#15859=CARTESIAN_POINT('Origin',(-1.55,-8.,5.77));
#15860=CARTESIAN_POINT('Origin',(-1.55,-8.,5.77));
#19298=UNCERTAINTY_MEASURE_WITH_UNIT(LENGTH_MEASURE(0.001),#19362,
'DISTANCE_ACCURACY_VALUE',
'Maximum model space distance between geometric entities at asserted c
onnectivities');
#19323=UNCERTAINTY_MEASURE_WITH_UNIT(LENGTH_MEASURE(0.001),#19362,
'DISTANCE_ACCURACY_VALUE',
'Maximum model space distance between geometric entities at asserted c
onnectivities');
#19336=(
GEOMETRIC_REPRESENTATION_CONTEXT(3)
GLOBAL_UNCERTAINTY_ASSIGNED_CONTEXT((#19298))
GLOBAL_UNIT_ASSIGNED_CONTEXT((#19362,#19364,#19365))
REPRESENTATION_CONTEXT('','3D')
);
#19361=(
GEOMETRIC_REPRESENTATION_CONTEXT(3)
GLOBAL_UNCERTAINTY_ASSIGNED_CONTEXT((#19323))
GLOBAL_UNIT_ASSIGNED_CONTEXT((#19362,#19364,#19365))
REPRESENTATION_CONTEXT('','3D')
);
#19362=(
LENGTH_UNIT()
NAMED_UNIT(*)
SI_UNIT(.CENTI.,.METRE.)
);
#19364=(
NAMED_UNIT(*)
PLANE_ANGLE_UNIT()
SI_UNIT($,.RADIAN.)
);
#19365=(
NAMED_UNIT(*)
SI_UNIT($,.STERADIAN.)
SOLID_ANGLE_UNIT()
);
#19378=SHAPE_DEFINITION_REPRESENTATION(#19415,#19500);
#19415=PRODUCT_DEFINITION_SHAPE('',$,#19538);
#19500=SHAPE_REPRESENTATION('',(#11527),#19336);
#19525=PRODUCT_DEFINITION_CONTEXT('part definition',#19638,'design');
#19538=PRODUCT_DEFINITION('M3x10 motor screw (1)','M3x10 motor screw (1)',
#19575,#19525);
#19575=PRODUCT_DEFINITION_FORMATION('',$,#19652);
#19638=APPLICATION_CONTEXT(
'Core Data for Automotive Mechanical Design Process');
#19639=PRODUCT_CONTEXT('part definition',#19638,'mechanical');
#19652=PRODUCT('M3x10 motor screw (1)','M3x10 motor screw (1)',
'M3x10 motor screw (1)',(#19639));
#19747=COLOUR_RGB('Black',0.12,0.14,0.17);
#19748=FILL_AREA_STYLE_COLOUR('',#19747);
#19749=FILL_AREA_STYLE('',(#19748));
#19750=SURFACE_STYLE_FILL_AREA(#19749);
#19751=SURFACE_SIDE_STYLE('',(#19750));
#19752=SURFACE_STYLE_USAGE(.BOTH.,#19751);
#19753=PRESENTATION_STYLE_ASSIGNMENT((#19752));
ENDSEC;
END-ISO-10303-21;
